ISO-10303-21;
HEADER;
/* Generated by software containing ST-Developer
 * from STEP Tools, Inc. (www.steptools.com) 
 */

FILE_DESCRIPTION(
/* description */ ('Hinged panel with latch'),
/* implementation_level */ '2;1');

FILE_NAME(
/* name */ 'Cap Screw - M5x20.step',
/* time_stamp */ '2026-10-27T20:36:01-07:00',
/* author */ (''),
/* organization */ (''),
/* preprocessor_version */ 'ST-DEVELOPER v20.2',
/* originating_system */ 'Autodesk Translation Framework v15.17.0.0',
/* authorisation */ '');

FILE_SCHEMA (('AUTOMOTIVE_DESIGN { 1 0 10303 214 3 1 1 }'));
ENDSEC;

DATA;
#10=MECHANICAL_DESIGN_GEOMETRIC_PRESENTATION_REPRESENTATION('',(#309),#6743);
#233=ORIENTED_CLOSED_SHELL('',*,#3814,.F.);
#236=BREP_WITH_VOIDS('Body1',#3813,(#233));
#252=CONICAL_SURFACE('',#4296,0.4,0.785398163397448);
#253=CONICAL_SURFACE('',#4300,0.41,0.785398163397448);
#254=CONICAL_SURFACE('',#4304,0.26,0.463647609000806);
#255=CONICAL_SURFACE('',#4308,0.225,0.785398163397448);
#277=SHAPE_REPRESENTATION_RELATIONSHIP('SRR','None',#6853,#293);
#293=ADVANCED_BREP_SHAPE_REPRESENTATION('',(#236),#6739);
#309=STYLED_ITEM('',(#7010),#236);
#367=FACE_BOUND('',#947,.T.);
#498=PLANE('',#4294);
#499=PLANE('',#4302);
#500=PLANE('',#4310);
#501=PLANE('',#4311);
#502=PLANE('',#4312);
#503=PLANE('',#4313);
#504=PLANE('',#4314);
#505=PLANE('',#4315);
#506=PLANE('',#4316);
#507=PLANE('',#4317);
#508=PLANE('',#4318);
#694=FACE_OUTER_BOUND('',#942,.T.);
#695=FACE_OUTER_BOUND('',#943,.T.);
#696=FACE_OUTER_BOUND('',#944,.T.);
#697=FACE_OUTER_BOUND('',#945,.T.);
#698=FACE_OUTER_BOUND('',#946,.T.);
#699=FACE_OUTER_BOUND('',#948,.T.);
#700=FACE_OUTER_BOUND('',#949,.T.);
#701=FACE_OUTER_BOUND('',#950,.T.);
#702=FACE_OUTER_BOUND('',#951,.T.);
#703=FACE_OUTER_BOUND('',#952,.T.);
#704=FACE_OUTER_BOUND('',#953,.T.);
#705=FACE_OUTER_BOUND('',#954,.T.);
#706=FACE_OUTER_BOUND('',#955,.T.);
#707=FACE_OUTER_BOUND('',#956,.T.);
#708=FACE_OUTER_BOUND('',#957,.T.);
#709=FACE_OUTER_BOUND('',#958,.T.);
#710=FACE_OUTER_BOUND('',#959,.T.);
#942=EDGE_LOOP('',(#3412));
#943=EDGE_LOOP('',(#3413,#3414,#3415,#3416));
#944=EDGE_LOOP('',(#3417,#3418,#3419,#3420));
#945=EDGE_LOOP('',(#3421,#3422,#3423,#3424));
#946=EDGE_LOOP('',(#3425));
#947=EDGE_LOOP('',(#3426));
#948=EDGE_LOOP('',(#3427,#3428,#3429,#3430));
#949=EDGE_LOOP('',(#3431,#3432,#3433,#3434));
#950=EDGE_LOOP('',(#3435,#3436,#3437,#3438));
#951=EDGE_LOOP('',(#3439));
#952=EDGE_LOOP('',(#3440,#3441,#3442,#3443));
#953=EDGE_LOOP('',(#3444,#3445,#3446,#3447));
#954=EDGE_LOOP('',(#3448,#3449,#3450,#3451));
#955=EDGE_LOOP('',(#3452,#3453,#3454,#3455));
#956=EDGE_LOOP('',(#3456,#3457,#3458,#3459));
#957=EDGE_LOOP('',(#3460,#3461,#3462,#3463));
#958=EDGE_LOOP('',(#3464,#3465,#3466,#3467,#3468,#3469));
#959=EDGE_LOOP('',(#3470,#3471,#3472,#3473,#3474,#3475));
#1294=LINE('',#6510,#1652);
#1295=LINE('',#6514,#1653);
#1296=LINE('',#6518,#1654);
#1297=LINE('',#6525,#1655);
#1298=LINE('',#6529,#1656);
#1299=LINE('',#6533,#1657);
#1300=LINE('',#6538,#1658);
#1301=LINE('',#6540,#1659);
#1302=LINE('',#6542,#1660);
#1303=LINE('',#6543,#1661);
#1304=LINE('',#6546,#1662);
#1305=LINE('',#6548,#1663);
#1306=LINE('',#6549,#1664);
#1307=LINE('',#6552,#1665);
#1308=LINE('',#6554,#1666);
#1309=LINE('',#6555,#1667);
#1310=LINE('',#6558,#1668);
#1311=LINE('',#6560,#1669);
#1312=LINE('',#6561,#1670);
#1313=LINE('',#6564,#1671);
#1314=LINE('',#6566,#1672);
#1315=LINE('',#6567,#1673);
#1316=LINE('',#6569,#1674);
#1317=LINE('',#6570,#1675);
#1652=VECTOR('',#5284,0.4);
#1653=VECTOR('',#5289,0.425);
#1654=VECTOR('',#5294,0.41);
#1655=VECTOR('',#5303,0.26);
#1656=VECTOR('',#5308,0.25);
#1657=VECTOR('',#5313,0.225);
#1658=VECTOR('',#5318,1.);
#1659=VECTOR('',#5319,1.);
#1660=VECTOR('',#5320,1.);
#1661=VECTOR('',#5321,1.);
#1662=VECTOR('',#5324,1.);
#1663=VECTOR('',#5325,1.);
#1664=VECTOR('',#5326,1.);
#1665=VECTOR('',#5329,1.);
#1666=VECTOR('',#5330,1.);
#1667=VECTOR('',#5331,1.);
#1668=VECTOR('',#5334,1.);
#1669=VECTOR('',#5335,1.);
#1670=VECTOR('',#5336,1.);
#1671=VECTOR('',#5339,1.);
#1672=VECTOR('',#5340,1.);
#1673=VECTOR('',#5341,1.);
#1674=VECTOR('',#5344,1.);
#1675=VECTOR('',#5345,1.);
#1777=CIRCLE('',#4295,0.375);
#1778=CIRCLE('',#4297,0.425);
#1779=CIRCLE('',#4299,0.425);
#1780=CIRCLE('',#4301,0.395);
#1781=CIRCLE('',#4303,0.27);
#1782=CIRCLE('',#4305,0.24505);
#1783=CIRCLE('',#4307,0.24505);
#1784=CIRCLE('',#4309,0.2);
#2061=VERTEX_POINT('',#6505);
#2062=VERTEX_POINT('',#6508);
#2063=VERTEX_POINT('',#6512);
#2064=VERTEX_POINT('',#6516);
#2065=VERTEX_POINT('',#6520);
#2066=VERTEX_POINT('',#6523);
#2067=VERTEX_POINT('',#6527);
#2068=VERTEX_POINT('',#6531);
#2069=VERTEX_POINT('',#6536);
#2070=VERTEX_POINT('',#6537);
#2071=VERTEX_POINT('',#6539);
#2072=VERTEX_POINT('',#6541);
#2073=VERTEX_POINT('',#6545);
#2074=VERTEX_POINT('',#6547);
#2075=VERTEX_POINT('',#6551);
#2076=VERTEX_POINT('',#6553);
#2077=VERTEX_POINT('',#6557);
#2078=VERTEX_POINT('',#6559);
#2079=VERTEX_POINT('',#6563);
#2080=VERTEX_POINT('',#6565);
#2518=EDGE_CURVE('',#2061,#2061,#1777,.T.);
#2519=EDGE_CURVE('',#2062,#2062,#1778,.T.);
#2520=EDGE_CURVE('',#2062,#2061,#1294,.T.);
#2521=EDGE_CURVE('',#2063,#2063,#1779,.T.);
#2522=EDGE_CURVE('',#2063,#2062,#1295,.T.);
#2523=EDGE_CURVE('',#2064,#2064,#1780,.T.);
#2524=EDGE_CURVE('',#2064,#2063,#1296,.T.);
#2525=EDGE_CURVE('',#2065,#2065,#1781,.T.);
#2526=EDGE_CURVE('',#2066,#2066,#1782,.F.);
#2527=EDGE_CURVE('',#2066,#2065,#1297,.T.);
#2528=EDGE_CURVE('',#2067,#2067,#1783,.F.);
#2529=EDGE_CURVE('',#2067,#2066,#1298,.T.);
#2530=EDGE_CURVE('',#2068,#2068,#1784,.T.);
#2531=EDGE_CURVE('',#2068,#2067,#1299,.T.);
#2532=EDGE_CURVE('',#2069,#2070,#1300,.T.);
#2533=EDGE_CURVE('',#2070,#2071,#1301,.T.);
#2534=EDGE_CURVE('',#2071,#2072,#1302,.T.);
#2535=EDGE_CURVE('',#2069,#2072,#1303,.T.);
#2536=EDGE_CURVE('',#2070,#2073,#1304,.T.);
#2537=EDGE_CURVE('',#2073,#2074,#1305,.T.);
#2538=EDGE_CURVE('',#2074,#2071,#1306,.T.);
#2539=EDGE_CURVE('',#2073,#2075,#1307,.T.);
#2540=EDGE_CURVE('',#2075,#2076,#1308,.T.);
#2541=EDGE_CURVE('',#2076,#2074,#1309,.T.);
#2542=EDGE_CURVE('',#2075,#2077,#1310,.T.);
#2543=EDGE_CURVE('',#2077,#2078,#1311,.T.);
#2544=EDGE_CURVE('',#2078,#2076,#1312,.T.);
#2545=EDGE_CURVE('',#2077,#2079,#1313,.T.);
#2546=EDGE_CURVE('',#2079,#2080,#1314,.T.);
#2547=EDGE_CURVE('',#2080,#2078,#1315,.T.);
#2548=EDGE_CURVE('',#2079,#2069,#1316,.T.);
#2549=EDGE_CURVE('',#2072,#2080,#1317,.T.);
#3412=ORIENTED_EDGE('',*,*,#2518,.F.);
#3413=ORIENTED_EDGE('',*,*,#2519,.F.);
#3414=ORIENTED_EDGE('',*,*,#2520,.T.);
#3415=ORIENTED_EDGE('',*,*,#2518,.T.);
#3416=ORIENTED_EDGE('',*,*,#2520,.F.);
#3417=ORIENTED_EDGE('',*,*,#2521,.F.);
#3418=ORIENTED_EDGE('',*,*,#2522,.T.);
#3419=ORIENTED_EDGE('',*,*,#2519,.T.);
#3420=ORIENTED_EDGE('',*,*,#2522,.F.);
#3421=ORIENTED_EDGE('',*,*,#2523,.F.);
#3422=ORIENTED_EDGE('',*,*,#2524,.T.);
#3423=ORIENTED_EDGE('',*,*,#2521,.T.);
#3424=ORIENTED_EDGE('',*,*,#2524,.F.);
#3425=ORIENTED_EDGE('',*,*,#2523,.T.);
#3426=ORIENTED_EDGE('',*,*,#2525,.F.);
#3427=ORIENTED_EDGE('',*,*,#2526,.F.);
#3428=ORIENTED_EDGE('',*,*,#2527,.T.);
#3429=ORIENTED_EDGE('',*,*,#2525,.T.);
#3430=ORIENTED_EDGE('',*,*,#2527,.F.);
#3431=ORIENTED_EDGE('',*,*,#2528,.F.);
#3432=ORIENTED_EDGE('',*,*,#2529,.T.);
#3433=ORIENTED_EDGE('',*,*,#2526,.T.);
#3434=ORIENTED_EDGE('',*,*,#2529,.F.);
#3435=ORIENTED_EDGE('',*,*,#2530,.F.);
#3436=ORIENTED_EDGE('',*,*,#2531,.T.);
#3437=ORIENTED_EDGE('',*,*,#2528,.T.);
#3438=ORIENTED_EDGE('',*,*,#2531,.F.);
#3439=ORIENTED_EDGE('',*,*,#2530,.T.);
#3440=ORIENTED_EDGE('',*,*,#2532,.T.);
#3441=ORIENTED_EDGE('',*,*,#2533,.T.);
#3442=ORIENTED_EDGE('',*,*,#2534,.T.);
#3443=ORIENTED_EDGE('',*,*,#2535,.F.);
#3444=ORIENTED_EDGE('',*,*,#2536,.T.);
#3445=ORIENTED_EDGE('',*,*,#2537,.T.);
#3446=ORIENTED_EDGE('',*,*,#2538,.T.);
#3447=ORIENTED_EDGE('',*,*,#2533,.F.);
#3448=ORIENTED_EDGE('',*,*,#2539,.T.);
#3449=ORIENTED_EDGE('',*,*,#2540,.T.);
#3450=ORIENTED_EDGE('',*,*,#2541,.T.);
#3451=ORIENTED_EDGE('',*,*,#2537,.F.);
#3452=ORIENTED_EDGE('',*,*,#2542,.T.);
#3453=ORIENTED_EDGE('',*,*,#2543,.T.);
#3454=ORIENTED_EDGE('',*,*,#2544,.T.);
#3455=ORIENTED_EDGE('',*,*,#2540,.F.);
#3456=ORIENTED_EDGE('',*,*,#2545,.T.);
#3457=ORIENTED_EDGE('',*,*,#2546,.T.);
#3458=ORIENTED_EDGE('',*,*,#2547,.T.);
#3459=ORIENTED_EDGE('',*,*,#2543,.F.);
#3460=ORIENTED_EDGE('',*,*,#2548,.T.);
#3461=ORIENTED_EDGE('',*,*,#2535,.T.);
#3462=ORIENTED_EDGE('',*,*,#2549,.T.);
#3463=ORIENTED_EDGE('',*,*,#2546,.F.);
#3464=ORIENTED_EDGE('',*,*,#2548,.F.);
#3465=ORIENTED_EDGE('',*,*,#2545,.F.);
#3466=ORIENTED_EDGE('',*,*,#2542,.F.);
#3467=ORIENTED_EDGE('',*,*,#2539,.F.);
#3468=ORIENTED_EDGE('',*,*,#2536,.F.);
#3469=ORIENTED_EDGE('',*,*,#2532,.F.);
#3470=ORIENTED_EDGE('',*,*,#2549,.F.);
#3471=ORIENTED_EDGE('',*,*,#2534,.F.);
#3472=ORIENTED_EDGE('',*,*,#2538,.F.);
#3473=ORIENTED_EDGE('',*,*,#2541,.F.);
#3474=ORIENTED_EDGE('',*,*,#2544,.F.);
#3475=ORIENTED_EDGE('',*,*,#2547,.F.);
#3588=CYLINDRICAL_SURFACE('',#4298,0.425);
#3589=CYLINDRICAL_SURFACE('',#4306,0.24505);
#3763=ADVANCED_FACE('',(#694),#498,.T.);
#3764=ADVANCED_FACE('',(#695),#252,.T.);
#3765=ADVANCED_FACE('',(#696),#3588,.T.);
#3766=ADVANCED_FACE('',(#697),#253,.T.);
#3767=ADVANCED_FACE('',(#698,#367),#499,.T.);
#3768=ADVANCED_FACE('',(#699),#254,.T.);
#3769=ADVANCED_FACE('',(#700),#3589,.T.);
#3770=ADVANCED_FACE('',(#701),#255,.T.);
#3771=ADVANCED_FACE('',(#702),#500,.T.);
#3772=ADVANCED_FACE('',(#703),#501,.F.);
#3773=ADVANCED_FACE('',(#704),#502,.F.);
#3774=ADVANCED_FACE('',(#705),#503,.F.);
#3775=ADVANCED_FACE('',(#706),#504,.F.);
#3776=ADVANCED_FACE('',(#707),#505,.F.);
#3777=ADVANCED_FACE('',(#708),#506,.F.);
#3778=ADVANCED_FACE('',(#709),#507,.F.);
#3779=ADVANCED_FACE('',(#710),#508,.F.);
#3813=CLOSED_SHELL('',(#3763,#3764,#3765,#3766,#3767,#3768,#3769,#3770,
#3771));
#3814=CLOSED_SHELL('',(#3772,#3773,#3774,#3775,#3776,#3777,#3778,#3779));
#4293=AXIS2_PLACEMENT_3D('',#6503,#5274,#5275);
#4294=AXIS2_PLACEMENT_3D('',#6504,#5276,#5277);
#4295=AXIS2_PLACEMENT_3D('',#6506,#5278,#5279);
#4296=AXIS2_PLACEMENT_3D('',#6507,#5280,#5281);
#4297=AXIS2_PLACEMENT_3D('',#6509,#5282,#5283);
#4298=AXIS2_PLACEMENT_3D('',#6511,#5285,#5286);
#4299=AXIS2_PLACEMENT_3D('',#6513,#5287,#5288);
#4300=AXIS2_PLACEMENT_3D('',#6515,#5290,#5291);
#4301=AXIS2_PLACEMENT_3D('',#6517,#5292,#5293);
#4302=AXIS2_PLACEMENT_3D('',#6519,#5295,#5296);
#4303=AXIS2_PLACEMENT_3D('',#6521,#5297,#5298);
#4304=AXIS2_PLACEMENT_3D('',#6522,#5299,#5300);
#4305=AXIS2_PLACEMENT_3D('',#6524,#5301,#5302);
#4306=AXIS2_PLACEMENT_3D('',#6526,#5304,#5305);
#4307=AXIS2_PLACEMENT_3D('',#6528,#5306,#5307);
#4308=AXIS2_PLACEMENT_3D('',#6530,#5309,#5310);
#4309=AXIS2_PLACEMENT_3D('',#6532,#5311,#5312);
#4310=AXIS2_PLACEMENT_3D('',#6534,#5314,#5315);
#4311=AXIS2_PLACEMENT_3D('',#6535,#5316,#5317);
#4312=AXIS2_PLACEMENT_3D('',#6544,#5322,#5323);
#4313=AXIS2_PLACEMENT_3D('',#6550,#5327,#5328);
#4314=AXIS2_PLACEMENT_3D('',#6556,#5332,#5333);
#4315=AXIS2_PLACEMENT_3D('',#6562,#5337,#5338);
#4316=AXIS2_PLACEMENT_3D('',#6568,#5342,#5343);
#4317=AXIS2_PLACEMENT_3D('',#6571,#5346,#5347);
#4318=AXIS2_PLACEMENT_3D('',#6572,#5348,#5349);
#5274=DIRECTION('axis',(0.,0.,1.));
#5275=DIRECTION('refdir',(1.,0.,0.));
#5276=DIRECTION('center_axis',(0.,1.,0.));
#5277=DIRECTION('ref_axis',(0.,0.,1.));
#5278=DIRECTION('center_axis',(0.,-1.,0.));
#5279=DIRECTION('ref_axis',(1.,0.,0.));
#5280=DIRECTION('center_axis',(0.,-1.,0.));
#5281=DIRECTION('ref_axis',(1.,0.,0.));
#5282=DIRECTION('center_axis',(0.,-1.,0.));
#5283=DIRECTION('ref_axis',(1.,0.,0.));
#5284=DIRECTION('',(0.707106781186548,0.707106781186547,8.65956056235493E-17));
#5285=DIRECTION('center_axis',(0.,-1.,0.));
#5286=DIRECTION('ref_axis',(1.,0.,0.));
#5287=DIRECTION('center_axis',(0.,-1.,0.));
#5288=DIRECTION('ref_axis',(1.,0.,0.));
#5289=DIRECTION('',(0.,1.,0.));
#5290=DIRECTION('center_axis',(0.,1.,0.));
#5291=DIRECTION('ref_axis',(1.,0.,0.));
#5292=DIRECTION('center_axis',(0.,-1.,0.));
#5293=DIRECTION('ref_axis',(1.,0.,0.));
#5294=DIRECTION('',(-0.707106781186547,0.707106781186548,-8.65956056235493E-17));
#5295=DIRECTION('center_axis',(0.,-1.,0.));
#5296=DIRECTION('ref_axis',(0.,0.,-1.));
#5297=DIRECTION('center_axis',(0.,-1.,0.));
#5298=DIRECTION('ref_axis',(1.,0.,0.));
#5299=DIRECTION('center_axis',(0.,1.,0.));
#5300=DIRECTION('ref_axis',(1.,0.,0.));
#5301=DIRECTION('center_axis',(0.,1.,0.));
#5302=DIRECTION('ref_axis',(1.,0.,0.));
#5303=DIRECTION('',(-0.447213595499958,0.894427190999916,-5.47678698264203E-17));
#5304=DIRECTION('center_axis',(0.,-1.,0.));
#5305=DIRECTION('ref_axis',(1.,0.,0.));
#5306=DIRECTION('center_axis',(0.,1.,0.));
#5307=DIRECTION('ref_axis',(1.,0.,0.));
#5308=DIRECTION('',(0.,1.,0.));
#5309=DIRECTION('center_axis',(0.,1.,0.));
#5310=DIRECTION('ref_axis',(1.,0.,0.));
#5311=DIRECTION('center_axis',(0.,-1.,0.));
#5312=DIRECTION('ref_axis',(1.,0.,0.));
#5313=DIRECTION('',(-0.707106781186547,0.707106781186548,-8.65956056235493E-17));
#5314=DIRECTION('center_axis',(0.,-1.,0.));
#5315=DIRECTION('ref_axis',(0.,0.,-1.));
#5316=DIRECTION('center_axis',(0.866025403784439,0.,-0.5));
#5317=DIRECTION('ref_axis',(0.5,0.,0.866025403784439));
#5318=DIRECTION('',(-0.5,0.,-0.866025403784439));
#5319=DIRECTION('',(0.,-1.,0.));
#5320=DIRECTION('',(0.5,0.,0.866025403784439));
#5321=DIRECTION('',(0.,-1.,0.));
#5322=DIRECTION('center_axis',(1.20185167898973E-16,0.,-1.));
#5323=DIRECTION('ref_axis',(1.,0.,1.20185167898973E-16));
#5324=DIRECTION('',(-1.,0.,-1.20185167898973E-16));
#5325=DIRECTION('',(0.,-1.,0.));
#5326=DIRECTION('',(1.,0.,1.20185167898973E-16));
#5327=DIRECTION('center_axis',(-0.866025403784439,0.,-0.5));
#5328=DIRECTION('ref_axis',(0.5,0.,-0.866025403784439));
#5329=DIRECTION('',(-0.5,0.,0.866025403784439));
#5330=DIRECTION('',(0.,-1.,0.));
#5331=DIRECTION('',(0.5,0.,-0.866025403784439));
#5332=DIRECTION('center_axis',(-0.866025403784439,0.,0.5));
#5333=DIRECTION('ref_axis',(-0.5,0.,-0.866025403784439));
#5334=DIRECTION('',(0.5,0.,0.866025403784439));
#5335=DIRECTION('',(0.,-1.,0.));
#5336=DIRECTION('',(-0.5,0.,-0.866025403784439));
#5337=DIRECTION('center_axis',(-2.40370335797945E-16,0.,1.));
#5338=DIRECTION('ref_axis',(-1.,0.,-2.40370335797945E-16));
#5339=DIRECTION('',(1.,0.,2.40370335797945E-16));
#5340=DIRECTION('',(0.,-1.,0.));
#5341=DIRECTION('',(-1.,0.,-2.40370335797945E-16));
#5342=DIRECTION('center_axis',(0.866025403784439,0.,0.5));
#5343=DIRECTION('ref_axis',(-0.5,0.,0.866025403784439));
#5344=DIRECTION('',(0.5,0.,-0.866025403784439));
#5345=DIRECTION('',(-0.5,0.,0.866025403784439));
#5346=DIRECTION('center_axis',(0.,1.,0.));
#5347=DIRECTION('ref_axis',(1.,0.,0.));
#5348=DIRECTION('center_axis',(0.,-1.,0.));
#5349=DIRECTION('ref_axis',(0.,0.,-1.));
#6503=CARTESIAN_POINT('',(0.,0.,0.));
#6504=CARTESIAN_POINT('Origin',(0.375,0.5,0.));
#6505=CARTESIAN_POINT('',(-0.375,0.5,-4.59242549680257E-17));
#6506=CARTESIAN_POINT('Origin',(0.,0.5,0.));
#6507=CARTESIAN_POINT('Origin',(0.,0.475,0.));
#6508=CARTESIAN_POINT('',(-0.425,0.45,-5.20474889637625E-17));
#6509=CARTESIAN_POINT('Origin',(0.,0.45,0.));
#6510=CARTESIAN_POINT('',(-0.4,0.475,-4.89858719658941E-17));
#6511=CARTESIAN_POINT('Origin',(0.,0.24,0.));
#6512=CARTESIAN_POINT('',(-0.425,0.0299999999999998,-5.20474889637625E-17));
#6513=CARTESIAN_POINT('Origin',(0.,0.0299999999999998,0.));
#6514=CARTESIAN_POINT('',(-0.425,0.24,-5.20474889637625E-17));
#6515=CARTESIAN_POINT('Origin',(0.,0.0150000000000001,0.));
#6516=CARTESIAN_POINT('',(-0.395,4.85722573273506E-17,-4.83735485663204E-17));
#6517=CARTESIAN_POINT('Origin',(0.,0.,0.));
#6518=CARTESIAN_POINT('',(-0.41,0.0150000000000001,-5.02105187650415E-17));
#6519=CARTESIAN_POINT('Origin',(0.27,0.,0.));
#6520=CARTESIAN_POINT('',(-0.27,0.,-3.30654635769785E-17));
#6521=CARTESIAN_POINT('Origin',(0.,0.,0.));
#6522=CARTESIAN_POINT('Origin',(0.,-0.02,0.));
#6523=CARTESIAN_POINT('',(-0.24505,-0.0498999999999999,3.00099698131059E-17));
#6524=CARTESIAN_POINT('Origin',(0.,-0.0498999999999999,0.));
#6525=CARTESIAN_POINT('',(-0.26,-0.02,-3.18408167778312E-17));
#6526=CARTESIAN_POINT('Origin',(0.,-0.995,0.));
#6527=CARTESIAN_POINT('',(-0.24505,-1.95495,3.00099698131059E-17));
#6528=CARTESIAN_POINT('Origin',(0.,-1.95495,0.));
#6529=CARTESIAN_POINT('',(-0.24505,-0.995,-3.00099698131059E-17));
#6530=CARTESIAN_POINT('Origin',(0.,-1.975,0.));
#6531=CARTESIAN_POINT('',(-0.2,-2.,-2.44929359829471E-17));
#6532=CARTESIAN_POINT('Origin',(0.,-2.,0.));
#6533=CARTESIAN_POINT('',(-0.225,-1.975,-2.75545529808154E-17));
#6534=CARTESIAN_POINT('Origin',(0.,-2.,0.));
#6535=CARTESIAN_POINT('Origin',(0.115470053837925,-0.5,-0.2));
#6536=CARTESIAN_POINT('',(0.23094010767585,-0.5,0.));
#6537=CARTESIAN_POINT('',(0.115470053837925,-0.5,-0.2));
#6538=CARTESIAN_POINT('',(0.23094010767585,-0.5,0.));
#6539=CARTESIAN_POINT('',(0.115470053837925,-0.8,-0.2));
#6540=CARTESIAN_POINT('',(0.115470053837925,-0.5,-0.2));
#6541=CARTESIAN_POINT('',(0.23094010767585,-0.8,0.));
#6542=CARTESIAN_POINT('',(0.23094010767585,-0.8,0.));
#6543=CARTESIAN_POINT('',(0.23094010767585,-0.5,0.));
#6544=CARTESIAN_POINT('Origin',(-0.115470053837925,-0.5,-0.2));
#6545=CARTESIAN_POINT('',(-0.115470053837925,-0.5,-0.2));
#6546=CARTESIAN_POINT('',(0.115470053837925,-0.5,-0.2));
#6547=CARTESIAN_POINT('',(-0.115470053837925,-0.8,-0.2));
#6548=CARTESIAN_POINT('',(-0.115470053837925,-0.5,-0.2));
#6549=CARTESIAN_POINT('',(0.115470053837925,-0.8,-0.2));
#6550=CARTESIAN_POINT('Origin',(-0.23094010767585,-0.5,-2.77555756156289E-17));
#6551=CARTESIAN_POINT('',(-0.23094010767585,-0.5,-2.82820063659975E-17));
#6552=CARTESIAN_POINT('',(-0.115470053837925,-0.5,-0.2));
#6553=CARTESIAN_POINT('',(-0.23094010767585,-0.8,-2.77555756156289E-17));
#6554=CARTESIAN_POINT('',(-0.23094010767585,-0.5,-2.82820063659975E-17));
#6555=CARTESIAN_POINT('',(-0.115470053837925,-0.8,-0.2));
#6556=CARTESIAN_POINT('Origin',(-0.115470053837925,-0.5,0.2));
#6557=CARTESIAN_POINT('',(-0.115470053837925,-0.5,0.2));
#6558=CARTESIAN_POINT('',(-0.23094010767585,-0.5,-2.82820063659975E-17));
#6559=CARTESIAN_POINT('',(-0.115470053837925,-0.8,0.2));
#6560=CARTESIAN_POINT('',(-0.115470053837925,-0.5,0.2));
#6561=CARTESIAN_POINT('',(-0.23094010767585,-0.8,-2.82820063659975E-17));
#6562=CARTESIAN_POINT('Origin',(0.115470053837925,-0.5,0.2));
#6563=CARTESIAN_POINT('',(0.115470053837925,-0.5,0.2));
#6564=CARTESIAN_POINT('',(-0.115470053837925,-0.5,0.2));
#6565=CARTESIAN_POINT('',(0.115470053837925,-0.8,0.2));
#6566=CARTESIAN_POINT('',(0.115470053837925,-0.5,0.2));
#6567=CARTESIAN_POINT('',(-0.115470053837925,-0.8,0.2));
#6568=CARTESIAN_POINT('Origin',(0.23094010767585,-0.5,0.));
#6569=CARTESIAN_POINT('',(0.115470053837925,-0.5,0.2));
#6570=CARTESIAN_POINT('',(0.115470053837925,-0.8,0.2));
#6571=CARTESIAN_POINT('Origin',(0.,-0.5,0.));
#6572=CARTESIAN_POINT('Origin',(0.,-0.8,0.));
#6718=UNCERTAINTY_MEASURE_WITH_UNIT(LENGTH_MEASURE(0.001),#6744,
'DISTANCE_ACCURACY_VALUE',
'Maximum model space distance between geometric entities at asserted c
onnectivities');
#6722=UNCERTAINTY_MEASURE_WITH_UNIT(LENGTH_MEASURE(0.001),#6744,
'DISTANCE_ACCURACY_VALUE',
'Maximum model space distance between geometric entities at asserted c
onnectivities');
#6739=(
GEOMETRIC_REPRESENTATION_CONTEXT(3)
GLOBAL_UNCERTAINTY_ASSIGNED_CONTEXT((#6718))
GLOBAL_UNIT_ASSIGNED_CONTEXT((#6744,#6746,#6747))
REPRESENTATION_CONTEXT('','3D')
);
#6743=(
GEOMETRIC_REPRESENTATION_CONTEXT(3)
GLOBAL_UNCERTAINTY_ASSIGNED_CONTEXT((#6722))
GLOBAL_UNIT_ASSIGNED_CONTEXT((#6744,#6746,#6747))
REPRESENTATION_CONTEXT('','3D')
);
#6744=(
LENGTH_UNIT()
NAMED_UNIT(*)
SI_UNIT(.CENTI.,.METRE.)
);
#6746=(
NAMED_UNIT(*)
PLANE_ANGLE_UNIT()
SI_UNIT($,.RADIAN.)
);
#6747=(
NAMED_UNIT(*)
SI_UNIT($,.STERADIAN.)
SOLID_ANGLE_UNIT()
);
#6764=SHAPE_DEFINITION_REPRESENTATION(#6815,#6853);
#6815=PRODUCT_DEFINITION_SHAPE('',$,#6874);
#6853=SHAPE_REPRESENTATION('',(#4293),#6739);
#6857=PRODUCT_DEFINITION_CONTEXT('part definition',#6919,'design');
#6874=PRODUCT_DEFINITION('Cap Screw - M5x20','Cap Screw - M5x20',#6894,
#6857);
#6894=PRODUCT_DEFINITION_FORMATION('',$,#6937);
#6919=APPLICATION_CONTEXT(
'Core Data for Automotive Mechanical Design Process');
#6920=PRODUCT_CONTEXT('part definition',#6919,'mechanical');
#6937=PRODUCT('Cap Screw - M5x20','Cap Screw - M5x20',
'Cap Screw - M5x20',(#6920));
#7004=COLOUR_RGB('Black',0.12,0.14,0.17);
#7005=FILL_AREA_STYLE_COLOUR('',#7004);
#7006=FILL_AREA_STYLE('',(#7005));
#7007=SURFACE_STYLE_FILL_AREA(#7006);
#7008=SURFACE_SIDE_STYLE('',(#7007));
#7009=SURFACE_STYLE_USAGE(.BOTH.,#7008);
#7010=PRESENTATION_STYLE_ASSIGNMENT((#7009));
ENDSEC;
END-ISO-10303-21;
